ISO-10303-21;
HEADER;
/* Generated by software containing ST-Developer
 * from STEP Tools, Inc. (www.steptools.com) 
 */

FILE_DESCRIPTION(
/* description */ ('Line shaft on three pillow blocks'),
/* implementation_level */ '2;1');

FILE_NAME(
/* name */ 'Mounting reducer bush (1).step',
/* time_stamp */ '2026-10-27T10:49:19-07:00',
/* author */ (''),
/* organization */ (''),
/* preprocessor_version */ 'ST-DEVELOPER v20.2',
/* originating_system */ 'Autodesk Translation Framework v15.17.0.0',
/* authorisation */ '');

FILE_SCHEMA (('AUTOMOTIVE_DESIGN { 1 0 10303 214 3 1 1 }'));
ENDSEC;

DATA;
#10=MECHANICAL_DESIGN_GEOMETRIC_PRESENTATION_REPRESENTATION('',(#344),#8377);
#290=SHAPE_REPRESENTATION_RELATIONSHIP('SRR','None',#8505,#317);
#317=ADVANCED_BREP_SHAPE_REPRESENTATION('',(#372),#8354);
#344=STYLED_ITEM('',(#8732),#372);
#372=MANIFOLD_SOLID_BREP('Body1',#4330);
#417=FACE_BOUND('',#987,.T.);
#418=FACE_BOUND('',#989,.T.);
#524=PLANE('',#4752);
#525=PLANE('',#4753);
#706=FACE_OUTER_BOUND('',#984,.T.);
#707=FACE_OUTER_BOUND('',#985,.T.);
#708=FACE_OUTER_BOUND('',#986,.T.);
#709=FACE_OUTER_BOUND('',#988,.T.);
#984=EDGE_LOOP('',(#3165,#3166,#3167,#3168));
#985=EDGE_LOOP('',(#3169,#3170,#3171,#3172));
#986=EDGE_LOOP('',(#3173));
#987=EDGE_LOOP('',(#3174));
#988=EDGE_LOOP('',(#3175));
#989=EDGE_LOOP('',(#3176));
#1331=LINE('',#6710,#1658);
#1332=LINE('',#6716,#1659);
#1658=VECTOR('',#5414,0.425);
#1659=VECTOR('',#5421,0.645);
#1941=CIRCLE('',#4747,0.425);
#1942=CIRCLE('',#4748,0.425);
#1943=CIRCLE('',#4750,0.645);
#1944=CIRCLE('',#4751,0.645);
#2140=VERTEX_POINT('',#6707);
#2141=VERTEX_POINT('',#6709);
#2142=VERTEX_POINT('',#6713);
#2143=VERTEX_POINT('',#6715);
#2531=EDGE_CURVE('',#2140,#2140,#1941,.T.);
#2532=EDGE_CURVE('',#2140,#2141,#1331,.T.);
#2533=EDGE_CURVE('',#2141,#2141,#1942,.T.);
#2534=EDGE_CURVE('',#2142,#2142,#1943,.T.);
#2535=EDGE_CURVE('',#2142,#2143,#1332,.T.);
#2536=EDGE_CURVE('',#2143,#2143,#1944,.T.);
#3165=ORIENTED_EDGE('',*,*,#2531,.F.);
#3166=ORIENTED_EDGE('',*,*,#2532,.T.);
#3167=ORIENTED_EDGE('',*,*,#2533,.T.);
#3168=ORIENTED_EDGE('',*,*,#2532,.F.);
#3169=ORIENTED_EDGE('',*,*,#2534,.F.);
#3170=ORIENTED_EDGE('',*,*,#2535,.T.);
#3171=ORIENTED_EDGE('',*,*,#2536,.T.);
#3172=ORIENTED_EDGE('',*,*,#2535,.F.);
#3173=ORIENTED_EDGE('',*,*,#2534,.T.);
#3174=ORIENTED_EDGE('',*,*,#2531,.T.);
#3175=ORIENTED_EDGE('',*,*,#2536,.F.);
#3176=ORIENTED_EDGE('',*,*,#2533,.F.);
#4017=CYLINDRICAL_SURFACE('',#4746,0.425);
#4018=CYLINDRICAL_SURFACE('',#4749,0.645);
#4124=ADVANCED_FACE('',(#706),#4017,.F.);
#4125=ADVANCED_FACE('',(#707),#4018,.T.);
#4126=ADVANCED_FACE('',(#708,#417),#524,.T.);
#4127=ADVANCED_FACE('',(#709,#418),#525,.F.);
#4330=CLOSED_SHELL('',(#4124,#4125,#4126,#4127));
#4745=AXIS2_PLACEMENT_3D('',#6705,#5408,#5409);
#4746=AXIS2_PLACEMENT_3D('',#6706,#5410,#5411);
#4747=AXIS2_PLACEMENT_3D('',#6708,#5412,#5413);
#4748=AXIS2_PLACEMENT_3D('',#6711,#5415,#5416);
#4749=AXIS2_PLACEMENT_3D('',#6712,#5417,#5418);
#4750=AXIS2_PLACEMENT_3D('',#6714,#5419,#5420);
#4751=AXIS2_PLACEMENT_3D('',#6717,#5422,#5423);
#4752=AXIS2_PLACEMENT_3D('',#6718,#5424,#5425);
#4753=AXIS2_PLACEMENT_3D('',#6719,#5426,#5427);
#5408=DIRECTION('axis',(0.,0.,1.));
#5409=DIRECTION('refdir',(1.,0.,0.));
#5410=DIRECTION('center_axis',(0.,0.,1.));
#5411=DIRECTION('ref_axis',(1.,0.,0.));
#5412=DIRECTION('center_axis',(0.,0.,-1.));
#5413=DIRECTION('ref_axis',(1.,0.,0.));
#5414=DIRECTION('',(0.,0.,-1.));
#5415=DIRECTION('center_axis',(0.,0.,-1.));
#5416=DIRECTION('ref_axis',(1.,0.,0.));
#5417=DIRECTION('center_axis',(0.,0.,1.));
#5418=DIRECTION('ref_axis',(1.,0.,0.));
#5419=DIRECTION('center_axis',(0.,0.,1.));
#5420=DIRECTION('ref_axis',(1.,0.,0.));
#5421=DIRECTION('',(0.,0.,-1.));
#5422=DIRECTION('center_axis',(0.,0.,1.));
#5423=DIRECTION('ref_axis',(1.,0.,0.));
#5424=DIRECTION('center_axis',(0.,0.,1.));
#5425=DIRECTION('ref_axis',(1.,0.,0.));
#5426=DIRECTION('center_axis',(0.,0.,1.));
#5427=DIRECTION('ref_axis',(1.,0.,0.));
#6705=CARTESIAN_POINT('',(0.,0.,0.));
#6706=CARTESIAN_POINT('Origin',(4.75,0.,1.2));
#6707=CARTESIAN_POINT('',(4.325,-5.20474889637625E-17,2.4));
#6708=CARTESIAN_POINT('Origin',(4.75,0.,2.4));
#6709=CARTESIAN_POINT('',(4.325,-5.20474889637625E-17,1.2));
#6710=CARTESIAN_POINT('',(4.325,-5.20474889637625E-17,1.2));
#6711=CARTESIAN_POINT('Origin',(4.75,0.,1.2));
#6712=CARTESIAN_POINT('Origin',(4.75,0.,1.2));
#6713=CARTESIAN_POINT('',(4.105,-7.89897185450042E-17,2.4));
#6714=CARTESIAN_POINT('Origin',(4.75,0.,2.4));
#6715=CARTESIAN_POINT('',(4.105,-7.89897185450042E-17,1.2));
#6716=CARTESIAN_POINT('',(4.105,-7.89897185450042E-17,1.2));
#6717=CARTESIAN_POINT('Origin',(4.75,0.,1.2));
#6718=CARTESIAN_POINT('Origin',(4.75,0.,2.4));
#6719=CARTESIAN_POINT('Origin',(4.75,0.,1.2));
#8322=UNCERTAINTY_MEASURE_WITH_UNIT(LENGTH_MEASURE(0.001),#8378,
'DISTANCE_ACCURACY_VALUE',
'Maximum model space distance between geometric entities at asserted c
onnectivities');
#8345=UNCERTAINTY_MEASURE_WITH_UNIT(LENGTH_MEASURE(0.001),#8378,
'DISTANCE_ACCURACY_VALUE',
'Maximum model space distance between geometric entities at asserted c
onnectivities');
#8354=(
GEOMETRIC_REPRESENTATION_CONTEXT(3)
GLOBAL_UNCERTAINTY_ASSIGNED_CONTEXT((#8322))
GLOBAL_UNIT_ASSIGNED_CONTEXT((#8378,#8380,#8381))
REPRESENTATION_CONTEXT('','3D')
);
#8377=(
GEOMETRIC_REPRESENTATION_CONTEXT(3)
GLOBAL_UNCERTAINTY_ASSIGNED_CONTEXT((#8345))
GLOBAL_UNIT_ASSIGNED_CONTEXT((#8378,#8380,#8381))
REPRESENTATION_CONTEXT('','3D')
);
#8378=(
LENGTH_UNIT()
NAMED_UNIT(*)
SI_UNIT(.CENTI.,.METRE.)
);
#8380=(
NAMED_UNIT(*)
PLANE_ANGLE_UNIT()
SI_UNIT($,.RADIAN.)
);
#8381=(
NAMED_UNIT(*)
SI_UNIT($,.STERADIAN.)
SOLID_ANGLE_UNIT()
);
#8390=SHAPE_DEFINITION_REPRESENTATION(#8421,#8505);
#8421=PRODUCT_DEFINITION_SHAPE('',$,#8537);
#8505=SHAPE_REPRESENTATION('',(#4745),#8354);
#8528=PRODUCT_DEFINITION_CONTEXT('part definition',#8623,'design');
#8537=PRODUCT_DEFINITION('Mounting reducer bush (1)',
'Mounting reducer bush (1)',#8568,#8528);
#8568=PRODUCT_DEFINITION_FORMATION('',$,#8633);
#8623=APPLICATION_CONTEXT(
'Core Data for Automotive Mechanical Design Process');
#8624=PRODUCT_CONTEXT('part definition',#8623,'mechanical');
#8633=PRODUCT('Mounting reducer bush (1)','Mounting reducer bush (1)',
'Mounting reducer bush (1)',(#8624));
#8726=COLOUR_RGB('Off White',0.89,0.88,0.83);
#8727=FILL_AREA_STYLE_COLOUR('',#8726);
#8728=FILL_AREA_STYLE('',(#8727));
#8729=SURFACE_STYLE_FILL_AREA(#8728);
#8730=SURFACE_SIDE_STYLE('',(#8729));
#8731=SURFACE_STYLE_USAGE(.BOTH.,#8730);
#8732=PRESENTATION_STYLE_ASSIGNMENT((#8731));
ENDSEC;
END-ISO-10303-21;
